ISO-10303-21;
HEADER;
/* Generated by software containing ST-Developer
 * from STEP Tools, Inc. (www.steptools.com) 
 */

FILE_DESCRIPTION(
/* description */ ('V-block with clamp strap'),
/* implementation_level */ '2;1');

FILE_NAME(
/* name */ 'Hex Nut - M5.step',
/* time_stamp */ '2026-10-27T10:50:53-07:00',
/* author */ (''),
/* organization */ (''),
/* preprocessor_version */ 'ST-DEVELOPER v20.2',
/* originating_system */ 'Autodesk Translation Framework v15.17.0.0',
/* authorisation */ '');

FILE_SCHEMA (('AUTOMOTIVE_DESIGN { 1 0 10303 214 3 1 1 }'));
ENDSEC;

DATA;
#10=MECHANICAL_DESIGN_GEOMETRIC_PRESENTATION_REPRESENTATION('',(#278),#7344);
#175=(
BOUNDED_CURVE()
B_SPLINE_CURVE(2,(#6900,#6901,#6902),.UNSPECIFIED.,.F.,.F.)
B_SPLINE_CURVE_WITH_KNOTS((3,3),(0.140651836354967,0.670383167684795),
 .UNSPECIFIED.)
CURVE()
GEOMETRIC_REPRESENTATION_ITEM()
RATIONAL_B_SPLINE_CURVE((1.11602540378444,1.28867513459481,1.11602540378444))
REPRESENTATION_ITEM('')
);
#176=(
BOUNDED_CURVE()
B_SPLINE_CURVE(2,(#6904,#6905,#6906),.UNSPECIFIED.,.F.,.F.)
B_SPLINE_CURVE_WITH_KNOTS((3,3),(0.140651836354967,0.670383167684795),
 .UNSPECIFIED.)
CURVE()
GEOMETRIC_REPRESENTATION_ITEM()
RATIONAL_B_SPLINE_CURVE((1.11602540378444,1.28867513459481,1.11602540378444))
REPRESENTATION_ITEM('')
);
#177=(
BOUNDED_CURVE()
B_SPLINE_CURVE(2,(#6911,#6912,#6913),.UNSPECIFIED.,.F.,.F.)
B_SPLINE_CURVE_WITH_KNOTS((3,3),(0.140651836354967,0.670383167684795),
 .UNSPECIFIED.)
CURVE()
GEOMETRIC_REPRESENTATION_ITEM()
RATIONAL_B_SPLINE_CURVE((1.11602540378444,1.28867513459481,1.11602540378444))
REPRESENTATION_ITEM('')
);
#178=(
BOUNDED_CURVE()
B_SPLINE_CURVE(2,(#6915,#6916,#6917),.UNSPECIFIED.,.F.,.F.)
B_SPLINE_CURVE_WITH_KNOTS((3,3),(0.140651836354967,0.670383167684795),
 .UNSPECIFIED.)
CURVE()
GEOMETRIC_REPRESENTATION_ITEM()
RATIONAL_B_SPLINE_CURVE((1.11602540378444,1.28867513459481,1.11602540378444))
REPRESENTATION_ITEM('')
);
#179=(
BOUNDED_CURVE()
B_SPLINE_CURVE(2,(#6919,#6920,#6921),.UNSPECIFIED.,.F.,.F.)
B_SPLINE_CURVE_WITH_KNOTS((3,3),(0.140651836354967,0.670383167684795),
 .UNSPECIFIED.)
CURVE()
GEOMETRIC_REPRESENTATION_ITEM()
RATIONAL_B_SPLINE_CURVE((1.11602540378444,1.28867513459481,1.11602540378444))
REPRESENTATION_ITEM('')
);
#180=(
BOUNDED_CURVE()
B_SPLINE_CURVE(2,(#6922,#6923,#6924),.UNSPECIFIED.,.F.,.F.)
B_SPLINE_CURVE_WITH_KNOTS((3,3),(0.140651836354967,0.670383167684795),
 .UNSPECIFIED.)
CURVE()
GEOMETRIC_REPRESENTATION_ITEM()
RATIONAL_B_SPLINE_CURVE((1.11602540378444,1.28867513459481,1.11602540378444))
REPRESENTATION_ITEM('')
);
#181=(
BOUNDED_CURVE()
B_SPLINE_CURVE(2,(#6931,#6932,#6933),.UNSPECIFIED.,.F.,.F.)
B_SPLINE_CURVE_WITH_KNOTS((3,3),(0.140651836354967,0.670383167684795),
 .UNSPECIFIED.)
CURVE()
GEOMETRIC_REPRESENTATION_ITEM()
RATIONAL_B_SPLINE_CURVE((1.11602540378444,1.28867513459481,1.11602540378444))
REPRESENTATION_ITEM('')
);
#182=(
BOUNDED_CURVE()
B_SPLINE_CURVE(2,(#6935,#6936,#6937),.UNSPECIFIED.,.F.,.F.)
B_SPLINE_CURVE_WITH_KNOTS((3,3),(0.140651836354967,0.670383167684796),
 .UNSPECIFIED.)
CURVE()
GEOMETRIC_REPRESENTATION_ITEM()
RATIONAL_B_SPLINE_CURVE((1.11602540378444,1.28867513459481,1.11602540378444))
REPRESENTATION_ITEM('')
);
#183=(
BOUNDED_CURVE()
B_SPLINE_CURVE(2,(#6939,#6940,#6941),.UNSPECIFIED.,.F.,.F.)
B_SPLINE_CURVE_WITH_KNOTS((3,3),(0.140651836354967,0.670383167684795),
 .UNSPECIFIED.)
CURVE()
GEOMETRIC_REPRESENTATION_ITEM()
RATIONAL_B_SPLINE_CURVE((1.11602540378444,1.28867513459481,1.11602540378444))
REPRESENTATION_ITEM('')
);
#184=(
BOUNDED_CURVE()
B_SPLINE_CURVE(2,(#6943,#6944,#6945),.UNSPECIFIED.,.F.,.F.)
B_SPLINE_CURVE_WITH_KNOTS((3,3),(0.140651836354967,0.670383167684795),
 .UNSPECIFIED.)
CURVE()
GEOMETRIC_REPRESENTATION_ITEM()
RATIONAL_B_SPLINE_CURVE((1.11602540378444,1.28867513459482,1.11602540378444))
REPRESENTATION_ITEM('')
);
#185=(
BOUNDED_CURVE()
B_SPLINE_CURVE(2,(#6947,#6948,#6949),.UNSPECIFIED.,.F.,.F.)
B_SPLINE_CURVE_WITH_KNOTS((3,3),(0.140651836354967,0.670383167684795),
 .UNSPECIFIED.)
CURVE()
GEOMETRIC_REPRESENTATION_ITEM()
RATIONAL_B_SPLINE_CURVE((1.11602540378444,1.28867513459481,1.11602540378444))
REPRESENTATION_ITEM('')
);
#186=(
BOUNDED_CURVE()
B_SPLINE_CURVE(2,(#6950,#6951,#6952),.UNSPECIFIED.,.F.,.F.)
B_SPLINE_CURVE_WITH_KNOTS((3,3),(0.140651836354967,0.670383167684795),
 .UNSPECIFIED.)
CURVE()
GEOMETRIC_REPRESENTATION_ITEM()
RATIONAL_B_SPLINE_CURVE((1.11602540378444,1.28867513459481,1.11602540378444))
REPRESENTATION_ITEM('')
);
#210=CONICAL_SURFACE('',#4682,0.47094010767585,1.0471975511966);
#211=CONICAL_SURFACE('',#4684,0.47094010767585,1.0471975511966);
#236=SHAPE_REPRESENTATION_RELATIONSHIP('SRR','None',#7454,#257);
#257=ADVANCED_BREP_SHAPE_REPRESENTATION('',(#297),#7333);
#278=STYLED_ITEM('',(#7638),#297);
#297=MANIFOLD_SOLID_BREP('Body1',#4162);
#359=FACE_BOUND('',#1035,.T.);
#360=FACE_BOUND('',#1037,.T.);
#466=CIRCLE('',#4683,0.38);
#467=CIRCLE('',#4685,0.38);
#468=CIRCLE('',#4690,0.2117);
#469=CIRCLE('',#4691,0.2117);
#546=CYLINDRICAL_SURFACE('',#4689,0.2117);
#731=FACE_OUTER_BOUND('',#1025,.T.);
#732=FACE_OUTER_BOUND('',#1026,.T.);
#733=FACE_OUTER_BOUND('',#1027,.T.);
#734=FACE_OUTER_BOUND('',#1028,.T.);
#735=FACE_OUTER_BOUND('',#1029,.T.);
#736=FACE_OUTER_BOUND('',#1030,.T.);
#737=FACE_OUTER_BOUND('',#1031,.T.);
#738=FACE_OUTER_BOUND('',#1032,.T.);
#739=FACE_OUTER_BOUND('',#1033,.T.);
#740=FACE_OUTER_BOUND('',#1034,.T.);
#741=FACE_OUTER_BOUND('',#1036,.T.);
#1025=EDGE_LOOP('',(#3466,#3467,#3468,#3469,#3470,#3471,#3472,#3473,#3474));
#1026=EDGE_LOOP('',(#3475,#3476,#3477,#3478,#3479,#3480,#3481,#3482,#3483));
#1027=EDGE_LOOP('',(#3484,#3485,#3486,#3487));
#1028=EDGE_LOOP('',(#3488,#3489,#3490,#3491));
#1029=EDGE_LOOP('',(#3492,#3493,#3494,#3495));
#1030=EDGE_LOOP('',(#3496,#3497,#3498,#3499));
#1031=EDGE_LOOP('',(#3500,#3501,#3502,#3503));
#1032=EDGE_LOOP('',(#3504,#3505,#3506,#3507));
#1033=EDGE_LOOP('',(#3508,#3509,#3510,#3511));
#1034=EDGE_LOOP('',(#3512));
#1035=EDGE_LOOP('',(#3513));
#1036=EDGE_LOOP('',(#3514));
#1037=EDGE_LOOP('',(#3515));
#1404=LINE('',#6908,#1769);
#1405=LINE('',#6929,#1770);
#1406=LINE('',#6954,#1771);
#1407=LINE('',#6955,#1772);
#1408=LINE('',#6957,#1773);
#1409=LINE('',#6959,#1774);
#1410=LINE('',#6964,#1775);
#1411=LINE('',#6967,#1776);
#1412=LINE('',#6969,#1777);
#1769=VECTOR('',#5692,0.47094010767585);
#1770=VECTOR('',#5699,0.47094010767585);
#1771=VECTOR('',#5702,1.);
#1772=VECTOR('',#5703,1.);
#1773=VECTOR('',#5706,1.);
#1774=VECTOR('',#5709,1.);
#1775=VECTOR('',#5714,0.25);
#1776=VECTOR('',#5719,1.);
#1777=VECTOR('',#5722,1.);
#2085=VERTEX_POINT('',#6898);
#2086=VERTEX_POINT('',#6899);
#2087=VERTEX_POINT('',#6903);
#2088=VERTEX_POINT('',#6907);
#2089=VERTEX_POINT('',#6910);
#2090=VERTEX_POINT('',#6914);
#2091=VERTEX_POINT('',#6918);
#2092=VERTEX_POINT('',#6926);
#2093=VERTEX_POINT('',#6928);
#2094=VERTEX_POINT('',#6930);
#2095=VERTEX_POINT('',#6934);
#2096=VERTEX_POINT('',#6938);
#2097=VERTEX_POINT('',#6942);
#2098=VERTEX_POINT('',#6946);
#2099=VERTEX_POINT('',#6961);
#2100=VERTEX_POINT('',#6963);
#2559=EDGE_CURVE('',#2085,#2086,#175,.T.);
#2560=EDGE_CURVE('',#2087,#2085,#176,.T.);
#2561=EDGE_CURVE('',#2087,#2088,#1404,.T.);
#2562=EDGE_CURVE('',#2088,#2088,#466,.T.);
#2563=EDGE_CURVE('',#2089,#2087,#177,.T.);
#2564=EDGE_CURVE('',#2090,#2089,#178,.T.);
#2565=EDGE_CURVE('',#2091,#2090,#179,.T.);
#2566=EDGE_CURVE('',#2086,#2091,#180,.T.);
#2567=EDGE_CURVE('',#2092,#2092,#467,.T.);
#2568=EDGE_CURVE('',#2092,#2093,#1405,.T.);
#2569=EDGE_CURVE('',#2094,#2093,#181,.T.);
#2570=EDGE_CURVE('',#2095,#2094,#182,.T.);
#2571=EDGE_CURVE('',#2096,#2095,#183,.T.);
#2572=EDGE_CURVE('',#2097,#2096,#184,.T.);
#2573=EDGE_CURVE('',#2098,#2097,#185,.T.);
#2574=EDGE_CURVE('',#2093,#2098,#186,.T.);
#2575=EDGE_CURVE('',#2089,#2098,#1406,.T.);
#2576=EDGE_CURVE('',#2090,#2097,#1407,.T.);
#2577=EDGE_CURVE('',#2087,#2093,#1408,.T.);
#2578=EDGE_CURVE('',#2085,#2094,#1409,.T.);
#2579=EDGE_CURVE('',#2099,#2099,#468,.F.);
#2580=EDGE_CURVE('',#2099,#2100,#1410,.T.);
#2581=EDGE_CURVE('',#2100,#2100,#469,.F.);
#2582=EDGE_CURVE('',#2086,#2095,#1411,.T.);
#2583=EDGE_CURVE('',#2091,#2096,#1412,.T.);
#3466=ORIENTED_EDGE('',*,*,#2559,.F.);
#3467=ORIENTED_EDGE('',*,*,#2560,.F.);
#3468=ORIENTED_EDGE('',*,*,#2561,.T.);
#3469=ORIENTED_EDGE('',*,*,#2562,.F.);
#3470=ORIENTED_EDGE('',*,*,#2561,.F.);
#3471=ORIENTED_EDGE('',*,*,#2563,.F.);
#3472=ORIENTED_EDGE('',*,*,#2564,.F.);
#3473=ORIENTED_EDGE('',*,*,#2565,.F.);
#3474=ORIENTED_EDGE('',*,*,#2566,.F.);
#3475=ORIENTED_EDGE('',*,*,#2567,.F.);
#3476=ORIENTED_EDGE('',*,*,#2568,.T.);
#3477=ORIENTED_EDGE('',*,*,#2569,.F.);
#3478=ORIENTED_EDGE('',*,*,#2570,.F.);
#3479=ORIENTED_EDGE('',*,*,#2571,.F.);
#3480=ORIENTED_EDGE('',*,*,#2572,.F.);
#3481=ORIENTED_EDGE('',*,*,#2573,.F.);
#3482=ORIENTED_EDGE('',*,*,#2574,.F.);
#3483=ORIENTED_EDGE('',*,*,#2568,.F.);
#3484=ORIENTED_EDGE('',*,*,#2564,.T.);
#3485=ORIENTED_EDGE('',*,*,#2575,.T.);
#3486=ORIENTED_EDGE('',*,*,#2573,.T.);
#3487=ORIENTED_EDGE('',*,*,#2576,.F.);
#3488=ORIENTED_EDGE('',*,*,#2563,.T.);
#3489=ORIENTED_EDGE('',*,*,#2577,.T.);
#3490=ORIENTED_EDGE('',*,*,#2574,.T.);
#3491=ORIENTED_EDGE('',*,*,#2575,.F.);
#3492=ORIENTED_EDGE('',*,*,#2560,.T.);
#3493=ORIENTED_EDGE('',*,*,#2578,.T.);
#3494=ORIENTED_EDGE('',*,*,#2569,.T.);
#3495=ORIENTED_EDGE('',*,*,#2577,.F.);
#3496=ORIENTED_EDGE('',*,*,#2579,.F.);
#3497=ORIENTED_EDGE('',*,*,#2580,.T.);
#3498=ORIENTED_EDGE('',*,*,#2581,.T.);
#3499=ORIENTED_EDGE('',*,*,#2580,.F.);
#3500=ORIENTED_EDGE('',*,*,#2559,.T.);
#3501=ORIENTED_EDGE('',*,*,#2582,.T.);
#3502=ORIENTED_EDGE('',*,*,#2570,.T.);
#3503=ORIENTED_EDGE('',*,*,#2578,.F.);
#3504=ORIENTED_EDGE('',*,*,#2565,.T.);
#3505=ORIENTED_EDGE('',*,*,#2576,.T.);
#3506=ORIENTED_EDGE('',*,*,#2572,.T.);
#3507=ORIENTED_EDGE('',*,*,#2583,.F.);
#3508=ORIENTED_EDGE('',*,*,#2566,.T.);
#3509=ORIENTED_EDGE('',*,*,#2583,.T.);
#3510=ORIENTED_EDGE('',*,*,#2571,.T.);
#3511=ORIENTED_EDGE('',*,*,#2582,.F.);
#3512=ORIENTED_EDGE('',*,*,#2567,.T.);
#3513=ORIENTED_EDGE('',*,*,#2579,.T.);
#3514=ORIENTED_EDGE('',*,*,#2562,.T.);
#3515=ORIENTED_EDGE('',*,*,#2581,.F.);
#3860=PLANE('',#4686);
#3861=PLANE('',#4687);
#3862=PLANE('',#4688);
#3863=PLANE('',#4692);
#3864=PLANE('',#4693);
#3865=PLANE('',#4694);
#3866=PLANE('',#4695);
#3867=PLANE('',#4696);
#4077=ADVANCED_FACE('',(#731),#210,.T.);
#4078=ADVANCED_FACE('',(#732),#211,.T.);
#4079=ADVANCED_FACE('',(#733),#3860,.T.);
#4080=ADVANCED_FACE('',(#734),#3861,.T.);
#4081=ADVANCED_FACE('',(#735),#3862,.T.);
#4082=ADVANCED_FACE('',(#736),#546,.F.);
#4083=ADVANCED_FACE('',(#737),#3863,.T.);
#4084=ADVANCED_FACE('',(#738),#3864,.T.);
#4085=ADVANCED_FACE('',(#739),#3865,.T.);
#4086=ADVANCED_FACE('',(#740,#359),#3866,.T.);
#4087=ADVANCED_FACE('',(#741,#360),#3867,.F.);
#4162=CLOSED_SHELL('',(#4077,#4078,#4079,#4080,#4081,#4082,#4083,#4084,
#4085,#4086,#4087));
#4681=AXIS2_PLACEMENT_3D('',#6896,#5688,#5689);
#4682=AXIS2_PLACEMENT_3D('',#6897,#5690,#5691);
#4683=AXIS2_PLACEMENT_3D('',#6909,#5693,#5694);
#4684=AXIS2_PLACEMENT_3D('',#6925,#5695,#5696);
#4685=AXIS2_PLACEMENT_3D('',#6927,#5697,#5698);
#4686=AXIS2_PLACEMENT_3D('',#6953,#5700,#5701);
#4687=AXIS2_PLACEMENT_3D('',#6956,#5704,#5705);
#4688=AXIS2_PLACEMENT_3D('',#6958,#5707,#5708);
#4689=AXIS2_PLACEMENT_3D('',#6960,#5710,#5711);
#4690=AXIS2_PLACEMENT_3D('',#6962,#5712,#5713);
#4691=AXIS2_PLACEMENT_3D('',#6965,#5715,#5716);
#4692=AXIS2_PLACEMENT_3D('',#6966,#5717,#5718);
#4693=AXIS2_PLACEMENT_3D('',#6968,#5720,#5721);
#4694=AXIS2_PLACEMENT_3D('',#6970,#5723,#5724);
#4695=AXIS2_PLACEMENT_3D('',#6971,#5725,#5726);
#4696=AXIS2_PLACEMENT_3D('',#6972,#5727,#5728);
#5688=DIRECTION('axis',(0.,0.,1.));
#5689=DIRECTION('refdir',(1.,0.,0.));
#5690=DIRECTION('center_axis',(0.,1.,0.));
#5691=DIRECTION('ref_axis',(1.,0.,0.));
#5692=DIRECTION('',(0.866025403784439,-0.5,1.06057523872491E-16));
#5693=DIRECTION('center_axis',(0.,-1.,0.));
#5694=DIRECTION('ref_axis',(1.,0.,0.));
#5695=DIRECTION('center_axis',(0.,-1.,0.));
#5696=DIRECTION('ref_axis',(1.,0.,0.));
#5697=DIRECTION('center_axis',(0.,1.,0.));
#5698=DIRECTION('ref_axis',(1.,0.,0.));
#5699=DIRECTION('',(-0.866025403784439,-0.5,-1.06057523872491E-16));
#5700=DIRECTION('center_axis',(1.20185167898973E-16,0.,-1.));
#5701=DIRECTION('ref_axis',(-1.,0.,-1.20185167898973E-16));
#5702=DIRECTION('',(0.,1.,0.));
#5703=DIRECTION('',(0.,1.,0.));
#5704=DIRECTION('center_axis',(-0.866025403784439,0.,-0.5));
#5705=DIRECTION('ref_axis',(-0.5,0.,0.866025403784439));
#5706=DIRECTION('',(0.,1.,0.));
#5707=DIRECTION('center_axis',(-0.866025403784439,0.,0.5));
#5708=DIRECTION('ref_axis',(0.5,0.,0.866025403784439));
#5709=DIRECTION('',(0.,1.,0.));
#5710=DIRECTION('center_axis',(0.,1.,0.));
#5711=DIRECTION('ref_axis',(1.,0.,0.));
#5712=DIRECTION('center_axis',(0.,1.,0.));
#5713=DIRECTION('ref_axis',(1.,0.,0.));
#5714=DIRECTION('',(0.,-1.,0.));
#5715=DIRECTION('center_axis',(0.,1.,0.));
#5716=DIRECTION('ref_axis',(1.,0.,0.));
#5717=DIRECTION('center_axis',(-2.40370335797945E-16,0.,1.));
#5718=DIRECTION('ref_axis',(1.,0.,2.40370335797945E-16));
#5719=DIRECTION('',(0.,1.,0.));
#5720=DIRECTION('center_axis',(0.866025403784439,0.,-0.5));
#5721=DIRECTION('ref_axis',(-0.5,0.,-0.866025403784439));
#5722=DIRECTION('',(0.,1.,0.));
#5723=DIRECTION('center_axis',(0.866025403784439,0.,0.5));
#5724=DIRECTION('ref_axis',(0.5,0.,-0.866025403784439));
#5725=DIRECTION('center_axis',(0.,1.,0.));
#5726=DIRECTION('ref_axis',(1.,0.,0.));
#5727=DIRECTION('center_axis',(0.,1.,0.));
#5728=DIRECTION('ref_axis',(1.,0.,0.));
#6896=CARTESIAN_POINT('',(0.,0.,0.));
#6897=CARTESIAN_POINT('Origin',(0.,0.0525042956467857,0.));
#6898=CARTESIAN_POINT('',(-0.230940107675851,0.0472735643746089,0.4));
#6899=CARTESIAN_POINT('',(0.23094010767585,0.0472735643746089,0.4));
#6900=CARTESIAN_POINT('Ctrl Pts',(-0.230940107675851,0.0472735643746089,
0.4));
#6901=CARTESIAN_POINT('Ctrl Pts',(1.11022302462516E-16,-0.0193931022920578,
0.4));
#6902=CARTESIAN_POINT('Ctrl Pts',(0.23094010767585,0.0472735643746089,0.4));
#6903=CARTESIAN_POINT('',(-0.461880215351701,0.0472735643746089,-5.6564012731995E-17));
#6904=CARTESIAN_POINT('Ctrl Pts',(-0.461880215351701,0.0472735643746089,
-5.6564012731995E-17));
#6905=CARTESIAN_POINT('Ctrl Pts',(-0.346410161513776,-0.0193931022920579,
0.2));
#6906=CARTESIAN_POINT('Ctrl Pts',(-0.230940107675851,0.0472735643746089,
0.4));
#6907=CARTESIAN_POINT('',(-0.38,-2.08166817117217E-17,-4.65365783675994E-17));
#6908=CARTESIAN_POINT('',(-0.47094010767585,0.0525042956467857,-5.7673529545534E-17));
#6909=CARTESIAN_POINT('Origin',(0.,0.,0.));
#6910=CARTESIAN_POINT('',(-0.23094010767585,0.0472735643746089,-0.4));
#6911=CARTESIAN_POINT('Ctrl Pts',(-0.23094010767585,0.0472735643746089,
-0.4));
#6912=CARTESIAN_POINT('Ctrl Pts',(-0.346410161513775,-0.0193931022920578,
-0.2));
#6913=CARTESIAN_POINT('Ctrl Pts',(-0.461880215351701,0.0472735643746089,
-5.6564012731995E-17));
#6914=CARTESIAN_POINT('',(0.23094010767585,0.0472735643746089,-0.4));
#6915=CARTESIAN_POINT('Ctrl Pts',(0.23094010767585,0.0472735643746089,-0.4));
#6916=CARTESIAN_POINT('Ctrl Pts',(0.,-0.0193931022920578,-0.4));
#6917=CARTESIAN_POINT('Ctrl Pts',(-0.23094010767585,0.0472735643746089,
-0.4));
#6918=CARTESIAN_POINT('',(0.461880215351701,0.0472735643746089,0.));
#6919=CARTESIAN_POINT('Ctrl Pts',(0.461880215351701,0.0472735643746089,
0.));
#6920=CARTESIAN_POINT('Ctrl Pts',(0.346410161513776,-0.019393102292058,
-0.2));
#6921=CARTESIAN_POINT('Ctrl Pts',(0.23094010767585,0.0472735643746089,-0.4));
#6922=CARTESIAN_POINT('Ctrl Pts',(0.23094010767585,0.0472735643746089,0.4));
#6923=CARTESIAN_POINT('Ctrl Pts',(0.346410161513776,-0.0193931022920577,
0.2));
#6924=CARTESIAN_POINT('Ctrl Pts',(0.461880215351701,0.0472735643746089,
0.));
#6925=CARTESIAN_POINT('Origin',(0.,0.417495704353214,0.));
#6926=CARTESIAN_POINT('',(-0.38,0.47,-4.65365783675994E-17));
#6927=CARTESIAN_POINT('Origin',(0.,0.47,0.));
#6928=CARTESIAN_POINT('',(-0.461880215351701,0.422726435625391,-5.6564012731995E-17));
#6929=CARTESIAN_POINT('',(-0.47094010767585,0.417495704353214,-5.7673529545534E-17));
#6930=CARTESIAN_POINT('',(-0.230940107675851,0.422726435625391,0.4));
#6931=CARTESIAN_POINT('Ctrl Pts',(-0.230940107675851,0.422726435625391,
0.4));
#6932=CARTESIAN_POINT('Ctrl Pts',(-0.346410161513776,0.489393102292058,
0.2));
#6933=CARTESIAN_POINT('Ctrl Pts',(-0.461880215351701,0.422726435625391,
-5.6564012731995E-17));
#6934=CARTESIAN_POINT('',(0.23094010767585,0.422726435625391,0.4));
#6935=CARTESIAN_POINT('Ctrl Pts',(0.23094010767585,0.422726435625391,0.4));
#6936=CARTESIAN_POINT('Ctrl Pts',(8.32667268468867E-17,0.489393102292058,
0.4));
#6937=CARTESIAN_POINT('Ctrl Pts',(-0.230940107675851,0.422726435625391,
0.4));
#6938=CARTESIAN_POINT('',(0.461880215351701,0.422726435625391,0.));
#6939=CARTESIAN_POINT('Ctrl Pts',(0.461880215351701,0.422726435625391,0.));
#6940=CARTESIAN_POINT('Ctrl Pts',(0.346410161513776,0.489393102292058,0.2));
#6941=CARTESIAN_POINT('Ctrl Pts',(0.23094010767585,0.422726435625391,0.4));
#6942=CARTESIAN_POINT('',(0.23094010767585,0.422726435625391,-0.4));
#6943=CARTESIAN_POINT('Ctrl Pts',(0.23094010767585,0.422726435625391,-0.4));
#6944=CARTESIAN_POINT('Ctrl Pts',(0.346410161513775,0.489393102292058,-0.2));
#6945=CARTESIAN_POINT('Ctrl Pts',(0.461880215351701,0.422726435625391,0.));
#6946=CARTESIAN_POINT('',(-0.23094010767585,0.422726435625391,-0.4));
#6947=CARTESIAN_POINT('Ctrl Pts',(-0.23094010767585,0.422726435625391,-0.4));
#6948=CARTESIAN_POINT('Ctrl Pts',(-5.55111512312578E-17,0.489393102292058,
-0.4));
#6949=CARTESIAN_POINT('Ctrl Pts',(0.23094010767585,0.422726435625391,-0.4));
#6950=CARTESIAN_POINT('Ctrl Pts',(-0.461880215351701,0.422726435625391,
-5.6564012731995E-17));
#6951=CARTESIAN_POINT('Ctrl Pts',(-0.346410161513776,0.489393102292058,
-0.2));
#6952=CARTESIAN_POINT('Ctrl Pts',(-0.23094010767585,0.422726435625391,-0.4));
#6953=CARTESIAN_POINT('Origin',(0.23094010767585,0.,-0.4));
#6954=CARTESIAN_POINT('',(-0.23094010767585,0.,-0.4));
#6955=CARTESIAN_POINT('',(0.23094010767585,0.,-0.4));
#6956=CARTESIAN_POINT('Origin',(-0.23094010767585,0.,-0.4));
#6957=CARTESIAN_POINT('',(-0.461880215351701,0.,-5.6564012731995E-17));
#6958=CARTESIAN_POINT('Origin',(-0.461880215351701,0.,-5.6564012731995E-17));
#6959=CARTESIAN_POINT('',(-0.230940107675851,0.,0.4));
#6960=CARTESIAN_POINT('Origin',(0.,0.,0.));
#6961=CARTESIAN_POINT('',(-0.2117,0.47,2.59257727379495E-17));
#6962=CARTESIAN_POINT('Origin',(0.,0.47,0.));
#6963=CARTESIAN_POINT('',(-0.2117,0.,2.59257727379495E-17));
#6964=CARTESIAN_POINT('',(-0.2117,0.,2.59257727379495E-17));
#6965=CARTESIAN_POINT('Origin',(0.,0.,0.));
#6966=CARTESIAN_POINT('Origin',(-0.230940107675851,0.,0.4));
#6967=CARTESIAN_POINT('',(0.23094010767585,0.,0.4));
#6968=CARTESIAN_POINT('Origin',(0.461880215351701,0.,0.));
#6969=CARTESIAN_POINT('',(0.461880215351701,0.,0.));
#6970=CARTESIAN_POINT('Origin',(0.23094010767585,0.,0.4));
#6971=CARTESIAN_POINT('Origin',(0.,0.47,0.));
#6972=CARTESIAN_POINT('Origin',(0.,0.,0.));
#7307=UNCERTAINTY_MEASURE_WITH_UNIT(LENGTH_MEASURE(0.001),#7345,
'DISTANCE_ACCURACY_VALUE',
'Maximum model space distance between geometric entities at asserted c
onnectivities');
#7318=UNCERTAINTY_MEASURE_WITH_UNIT(LENGTH_MEASURE(0.001),#7345,
'DISTANCE_ACCURACY_VALUE',
'Maximum model space distance between geometric entities at asserted c
onnectivities');
#7333=(
GEOMETRIC_REPRESENTATION_CONTEXT(3)
GLOBAL_UNCERTAINTY_ASSIGNED_CONTEXT((#7307))
GLOBAL_UNIT_ASSIGNED_CONTEXT((#7345,#7347,#7348))
REPRESENTATION_CONTEXT('','3D')
);
#7344=(
GEOMETRIC_REPRESENTATION_CONTEXT(3)
GLOBAL_UNCERTAINTY_ASSIGNED_CONTEXT((#7318))
GLOBAL_UNIT_ASSIGNED_CONTEXT((#7345,#7347,#7348))
REPRESENTATION_CONTEXT('','3D')
);
#7345=(
LENGTH_UNIT()
NAMED_UNIT(*)
SI_UNIT(.CENTI.,.METRE.)
);
#7347=(
NAMED_UNIT(*)
PLANE_ANGLE_UNIT()
SI_UNIT($,.RADIAN.)
);
#7348=(
NAMED_UNIT(*)
SI_UNIT($,.STERADIAN.)
SOLID_ANGLE_UNIT()
);
#7363=SHAPE_DEFINITION_REPRESENTATION(#7388,#7454);
#7388=PRODUCT_DEFINITION_SHAPE('',$,#7480);
#7454=SHAPE_REPRESENTATION('',(#4681),#7333);
#7465=PRODUCT_DEFINITION_CONTEXT('part definition',#7542,'design');
#7480=PRODUCT_DEFINITION('Hex Nut - M5','Hex Nut - M5',#7505,#7465);
#7505=PRODUCT_DEFINITION_FORMATION('',$,#7558);
#7542=APPLICATION_CONTEXT(
'Core Data for Automotive Mechanical Design Process');
#7543=PRODUCT_CONTEXT('part definition',#7542,'mechanical');
#7558=PRODUCT('Hex Nut - M5','Hex Nut - M5','Hex Nut - M5',(#7543));
#7632=COLOUR_RGB('Black',0.12,0.14,0.17);
#7633=FILL_AREA_STYLE_COLOUR('',#7632);
#7634=FILL_AREA_STYLE('',(#7633));
#7635=SURFACE_STYLE_FILL_AREA(#7634);
#7636=SURFACE_SIDE_STYLE('',(#7635));
#7637=SURFACE_STYLE_USAGE(.BOTH.,#7636);
#7638=PRESENTATION_STYLE_ASSIGNMENT((#7637));
ENDSEC;
END-ISO-10303-21;
